ISO-10303-21;
HEADER;
FILE_DESCRIPTION((''),'2;1');
FILE_NAME('Washer_2.step','2026-10-09T10:15:02-07:00',(''),(''),'','','');
FILE_SCHEMA (('AUTOMOTIVE_DESIGN { 1 0 10303 214 3 1 1 }'));
ENDSEC;
DATA;
#10=MECHANICAL_DESIGN_GEOMETRIC_PRESENTATION_REPRESENTATION('',(#86),#6779);
#66=SHAPE_REPRESENTATION_RELATIONSHIP('SRR','None',#6820,#76) ;
#76=ADVANCED_BREP_SHAPE_REPRESENTATION('',(#96),#6772) ;
#86=STYLED_ITEM('',(#6877),#96) ;
#96=MANIFOLD_SOLID_BREP('Body1',#3898) ;
#121=FACE_BOUND('',#764,.T.) ;
#122=FACE_BOUND('',#766,.T.) ;
#217=PLANE('',#4307) ;
#218=PLANE('',#4308) ;
#499=FACE_OUTER_BOUND('',#761,.T.) ;
#500=FACE_OUTER_BOUND('',#762,.T.) ;
#501=FACE_OUTER_BOUND('',#763,.T.) ;
#502=FACE_OUTER_BOUND('',#765,.T.) ;
#761=EDGE_LOOP('',(#3327,#3328,#3329,#3330)) ;
#762=EDGE_LOOP('',(#3331,#3332,#3333,#3334)) ;
#763=EDGE_LOOP('',(#3335)) ;
#764=EDGE_LOOP('',(#3336)) ;
#765=EDGE_LOOP('',(#3337)) ;
#766=EDGE_LOOP('',(#3338)) ;
#1117=LINE('',#6446,#1477) ;
#1118=LINE('',#6452,#1478) ;
#1477=VECTOR('',#5281,6.) ;
#1478=VECTOR('',#5288,3.2) ;
#1675=CIRCLE('',#4302,6.) ;
#1676=CIRCLE('',#4303,6.) ;
#1677=CIRCLE('',#4305,3.2) ;
#1678=CIRCLE('',#4306,3.2) ;
#1943=VERTEX_POINT('',#6443) ;
#1944=VERTEX_POINT('',#6445) ;
#1945=VERTEX_POINT('',#6449) ;
#1946=VERTEX_POINT('',#6451) ;
#2417=EDGE_CURVE('',#1943,#1943,#1675,.T.) ;
#2418=EDGE_CURVE('',#1943,#1944,#1117,.T.) ;
#2419=EDGE_CURVE('',#1944,#1944,#1676,.T.) ;
#2420=EDGE_CURVE('',#1945,#1945,#1677,.T.) ;
#2421=EDGE_CURVE('',#1945,#1946,#1118,.T.) ;
#2422=EDGE_CURVE('',#1946,#1946,#1678,.T.) ;
#3327=ORIENTED_EDGE('',*,*,#2417,.F.) ;
#3328=ORIENTED_EDGE('',*,*,#2418,.T.) ;
#3329=ORIENTED_EDGE('',*,*,#2419,.T.) ;
#3330=ORIENTED_EDGE('',*,*,#2418,.F.) ;
#3331=ORIENTED_EDGE('',*,*,#2420,.F.) ;
#3332=ORIENTED_EDGE('',*,*,#2421,.T.) ;
#3333=ORIENTED_EDGE('',*,*,#2422,.T.) ;
#3334=ORIENTED_EDGE('',*,*,#2421,.F.) ;
#3335=ORIENTED_EDGE('',*,*,#2419,.F.) ;
#3336=ORIENTED_EDGE('',*,*,#2420,.T.) ;
#3337=ORIENTED_EDGE('',*,*,#2417,.T.) ;
#3338=ORIENTED_EDGE('',*,*,#2422,.F.) ;
#3637=CYLINDRICAL_SURFACE('',#4301,6.) ;
#3638=CYLINDRICAL_SURFACE('',#4304,3.2) ;
#3823=ADVANCED_FACE('',(#499),#3637,.T.) ;
#3824=ADVANCED_FACE('',(#500),#3638,.F.) ;
#3825=ADVANCED_FACE('',(#501,#121),#217,.F.) ;
#3826=ADVANCED_FACE('',(#502,#122),#218,.T.) ;
#3898=CLOSED_SHELL('',(#3823,#3824,#3825,#3826)) ;
#4300=AXIS2_PLACEMENT_3D('',#6441,#5275,#5276) ;
#4301=AXIS2_PLACEMENT_3D('',#6442,#5277,#5278) ;
#4302=AXIS2_PLACEMENT_3D('',#6444,#5279,#5280) ;
#4303=AXIS2_PLACEMENT_3D('',#6447,#5282,#5283) ;
#4304=AXIS2_PLACEMENT_3D('',#6448,#5284,#5285) ;
#4305=AXIS2_PLACEMENT_3D('',#6450,#5286,#5287) ;
#4306=AXIS2_PLACEMENT_3D('',#6453,#5289,#5290) ;
#4307=AXIS2_PLACEMENT_3D('',#6454,#5291,#5292) ;
#4308=AXIS2_PLACEMENT_3D('',#6455,#5293,#5294) ;
#5275=DIRECTION('axis',(0.,0.,1.)) ;
#5276=DIRECTION('refdir',(1.,0.,0.)) ;
#5277=DIRECTION('center_axis',(0.,-1.,0.)) ;
#5278=DIRECTION('ref_axis',(1.,0.,0.)) ;
#5279=DIRECTION('center_axis',(0.,-1.,0.)) ;
#5280=DIRECTION('ref_axis',(0.,0.,1.)) ;
#5281=DIRECTION('',(0.,1.,0.)) ;
#5282=DIRECTION('center_axis',(0.,-1.,0.)) ;
#5283=DIRECTION('ref_axis',(0.,0.,1.)) ;
#5284=DIRECTION('center_axis',(0.,-1.,0.)) ;
#5285=DIRECTION('ref_axis',(1.,0.,0.)) ;
#5286=DIRECTION('center_axis',(0.,-1.,0.)) ;
#5287=DIRECTION('ref_axis',(0.,0.,1.)) ;
#5288=DIRECTION('',(0.,-1.,0.)) ;
#5289=DIRECTION('center_axis',(0.,-1.,0.)) ;
#5290=DIRECTION('ref_axis',(0.,0.,1.)) ;
#5291=DIRECTION('center_axis',(0.,-1.,0.)) ;
#5292=DIRECTION('ref_axis',(1.,0.,0.)) ;
#5293=DIRECTION('center_axis',(0.,-1.,0.)) ;
#5294=DIRECTION('ref_axis',(1.,0.,0.)) ;
#6441=CARTESIAN_POINT('',(0.,0.,0.)) ;
#6442=CARTESIAN_POINT('Origin',(-35.,-19.5,-10.)) ;
#6443=CARTESIAN_POINT('',(-41.,-20.,-10.)) ;
#6444=CARTESIAN_POINT('Origin',(-35.,-20.,-10.)) ;
#6445=CARTESIAN_POINT('',(-41.,-19.,-10.)) ;
#6446=CARTESIAN_POINT('',(-41.,-19.5,-10.)) ;
#6447=CARTESIAN_POINT('Origin',(-35.,-19.,-10.)) ;
#6448=CARTESIAN_POINT('Origin',(-35.,-19.5,-10.)) ;
#6449=CARTESIAN_POINT('',(-38.2,-19.,-10.)) ;
#6450=CARTESIAN_POINT('Origin',(-35.,-19.,-10.)) ;
#6451=CARTESIAN_POINT('',(-38.2,-20.,-10.)) ;
#6452=CARTESIAN_POINT('',(-38.2,-19.5,-10.)) ;
#6453=CARTESIAN_POINT('Origin',(-35.,-20.,-10.)) ;
#6454=CARTESIAN_POINT('Origin',(0.,-19.,0.)) ;
#6455=CARTESIAN_POINT('Origin',(0.,-20.,0.)) ;
#6760=UNCERTAINTY_MEASURE_WITH_UNIT(LENGTH_MEASURE(0.01),#6780,
'DISTANCE_ACCURACY_VALUE',
'Maximum model space distance between geometric entities at asserted c
onnectivities') ;
#6767=UNCERTAINTY_MEASURE_WITH_UNIT(LENGTH_MEASURE(0.01),#6780,
'DISTANCE_ACCURACY_VALUE',
'Maximum model space distance between geometric entities at asserted c
onnectivities') ;
#6772=(
GEOMETRIC_REPRESENTATION_CONTEXT(3)
GLOBAL_UNCERTAINTY_ASSIGNED_CONTEXT((#6760))
GLOBAL_UNIT_ASSIGNED_CONTEXT((#6780,#6782,#6783))
REPRESENTATION_CONTEXT('','3D')
) ;
#6779=(
GEOMETRIC_REPRESENTATION_CONTEXT(3)
GLOBAL_UNCERTAINTY_ASSIGNED_CONTEXT((#6767))
GLOBAL_UNIT_ASSIGNED_CONTEXT((#6780,#6782,#6783))
REPRESENTATION_CONTEXT('','3D')
) ;
#6780=(
LENGTH_UNIT()
NAMED_UNIT(*)
SI_UNIT(.MILLI.,.METRE.)
) ;
#6782=(
NAMED_UNIT(*)
PLANE_ANGLE_UNIT()
SI_UNIT($,.RADIAN.)
) ;
#6783=(
NAMED_UNIT(*)
SI_UNIT($,.STERADIAN.)
SOLID_ANGLE_UNIT()
) ;
#6788=SHAPE_DEFINITION_REPRESENTATION(#6799,#6820) ;
#6799=PRODUCT_DEFINITION_SHAPE('',$,#6832) ;
#6820=SHAPE_REPRESENTATION('',(#4300),#6772) ;
#6827=PRODUCT_DEFINITION_CONTEXT('part definition',#6862,'design') ;
#6832=PRODUCT_DEFINITION('Washer_2','Washer_2',#6843,#6827) ;
#6843=PRODUCT_DEFINITION_FORMATION('',$,#6868) ;
#6862=APPLICATION_CONTEXT(
'Core Data for Automotive Mechanical Design Process') ;
#6863=PRODUCT_CONTEXT('part definition',#6862,'mechanical') ;
#6868=PRODUCT('Washer_2','Washer_2',$,(#6863)) ;
#6877=PRESENTATION_STYLE_ASSIGNMENT((#6880)) ;
#6880=SURFACE_STYLE_USAGE(.BOTH.,#6883) ;
#6883=SURFACE_SIDE_STYLE('',(#6886)) ;
#6886=SURFACE_STYLE_FILL_AREA(#6889) ;
#6889=FILL_AREA_STYLE('Opaque(203,203,203)',(#6892)) ;
#6892=FILL_AREA_STYLE_COLOUR('Opaque(203,203,203)',#6895) ;
#6895=COLOUR_RGB('Opaque(203,203,203)', 0.31764706, 0.68627451, 0.89019608) ;
ENDSEC;
END-ISO-10303-21;
